ISO-10303-21;
HEADER;
FILE_DESCRIPTION (('STEP AP214'),
    '1' );
FILE_NAME ('Pivot Pin.step',
    '2026-10-09T14:10:49',
    ( '' ),
    ( '' ),
    'SwSTEP 2.0',
    'SolidWorks 2026',
    '' );
FILE_SCHEMA (( 'AUTOMOTIVE_DESIGN' ));
ENDSEC;

DATA;
#5=ORIENTED_EDGE ( 'NONE', *, *, #9450, .F. ) ;
#20=STYLED_ITEM ( 'NONE', ( #9424 ), #6575 ) ;
#73=DIRECTION ( 'NONE',  ( 0.000000000000000000, -1.000000000000000000, 0.000000000000000000 ) ) ;
#76=AXIS2_PLACEMENT_3D ( 'NONE', #2154, #5245, #12004 ) ;
#103=DIRECTION ( 'NONE',  ( -0.2035550397114870846, 0.000000000000000000, -0.9790635044817342925 ) ) ;
#186=CARTESIAN_POINT ( 'NONE',  ( -13.57684171658811678, 32.54247999999999763, -0.8078590638549644209 ) ) ;
#202=ORIENTED_EDGE ( 'NONE', *, *, #14570, .F. ) ;
#208=DIRECTION ( 'NONE',  ( 0.9767031480033349089, 0.000000000000000000, -0.2145948757085681391 ) ) ;
#278=DIRECTION ( 'NONE',  ( 0.000000000000000000, -1.000000000000000000, 0.000000000000000000 ) ) ;
#309=ORIENTED_EDGE ( 'NONE', *, *, #592, .F. ) ;
#381=CIRCLE ( 'NONE', #12045, 4.365625000000000533 ) ;
#592=EDGE_CURVE ( 'NONE', #19225, #19536, #1138, .T. ) ;
#636=ORIENTED_EDGE ( 'NONE', *, *, #7107, .T. ) ;
#803=ORIENTED_EDGE ( 'NONE', *, *, #7640, .T. ) ;
#851=EDGE_CURVE ( 'NONE', #6512, #12344, #17443, .T. ) ;
#862=FACE_BOUND ( 'NONE', #9935, .T. ) ;
#960=PLANE ( 'NONE',  #2143 ) ;
#975=CARTESIAN_POINT ( 'NONE',  ( -17.46249999999999858, 0.000000000000000000, 0.000000000000000000 ) ) ;
#984=FACE_OUTER_BOUND ( 'NONE', #3236, .T. ) ;
#1015=ORIENTED_EDGE ( 'NONE', *, *, #17671, .F. ) ;
#1022=( NAMED_UNIT ( * ) SI_UNIT ( $, .STERADIAN. ) SOLID_ANGLE_UNIT ( ) );
#1035=EDGE_CURVE ( 'NONE', #21341, #16128, #2915, .T. ) ;
#1072=ORIENTED_EDGE ( 'NONE', *, *, #9091, .F. ) ;
#1077=ORIENTED_EDGE ( 'NONE', *, *, #1035, .T. ) ;
#1088=ORIENTED_EDGE ( 'NONE', *, *, #10570, .F. ) ;
#1090=PLANE ( 'NONE',  #10337 ) ;
#1119=DIRECTION ( 'NONE',  ( 0.000000000000000000, -1.000000000000000000, 0.000000000000000000 ) ) ;
#1131=AXIS2_PLACEMENT_3D ( 'NONE', #9158, #5950, #7949 ) ;
#1138=CIRCLE ( 'NONE', #7141, 4.365625000000000533 ) ;
#1152=FACE_OUTER_BOUND ( 'NONE', #16617, .T. ) ;
#1257=CYLINDRICAL_SURFACE ( 'NONE', #20191, 5.357812499999999645 ) ;
#1268=DIRECTION ( 'NONE',  ( -0.1878280753562736327, -0.000000000000000000, -0.9822019212503905194 ) ) ;
#1369=DIRECTION ( 'NONE',  ( -0.9822019212503904084, 0.000000000000000000, 0.1878280753562735772 ) ) ;
#1379=FACE_OUTER_BOUND ( 'NONE', #20204, .T. ) ;
#1390=EDGE_LOOP ( 'NONE', ( #12121, #4724, #2657, #7632, #2322 ) ) ;
#1409=AXIS2_PLACEMENT_3D ( 'NONE', #14333, #21049, #10673 ) ;
#1487=EDGE_CURVE ( 'NONE', #20325, #10491, #6279, .T. ) ;
#1520=AXIS2_PLACEMENT_3D ( 'NONE', #3677, #8317, #4998 ) ;
#1545=ADVANCED_FACE ( 'NONE', ( #14488, #9707 ), #1090, .F. ) ;
#1706=PRODUCT_DEFINITION_FORMATION_WITH_SPECIFIED_SOURCE ( 'ANY', '', #14278, .NOT_KNOWN. ) ;
#1720=CYLINDRICAL_SURFACE ( 'NONE', #9198, 5.357812499999999645 ) ;
#1768=VERTEX_POINT ( 'NONE', #4947 ) ;
#1789=DIRECTION ( 'NONE',  ( 0.000000000000000000, -1.000000000000000000, 0.000000000000000000 ) ) ;
#1827=DIRECTION ( 'NONE',  ( 0.000000000000000000, -1.000000000000000000, 0.000000000000000000 ) ) ;
#1844=CARTESIAN_POINT ( 'NONE',  ( -17.46249999999999858, 33.73373999999999739, 0.000000000000000000 ) ) ;
#1907=EDGE_CURVE ( 'NONE', #4938, #8453, #17059, .T. ) ;
#2045=CARTESIAN_POINT ( 'NONE',  ( -22.33576604192310455, 5.149960319306146062E-16, 0.9319226134156144425 ) ) ;
#2134=CIRCLE ( 'NONE', #7393, 3.175000000000001155 ) ;
#2143=AXIS2_PLACEMENT_3D ( 'NONE', #7385, #7710, #14470 ) ;
#2144=CARTESIAN_POINT ( 'NONE',  ( -17.46249999999999858, -1.587500000000002132, 0.000000000000000000 ) ) ;
#2154=CARTESIAN_POINT ( 'NONE',  ( -17.46249999999999858, 33.73373999999999739, 0.000000000000000000 ) ) ;
#2208=ADVANCED_FACE ( 'NONE', ( #7808 ), #5924, .T. ) ;
#2234=AXIS2_PLACEMENT_3D ( 'NONE', #14022, #2275, #17644 ) ;
#2275=DIRECTION ( 'NONE',  ( 0.000000000000000000, 0.000000000000000000, 1.000000000000000000 ) ) ;
#2322=ORIENTED_EDGE ( 'NONE', *, *, #1035, .F. ) ;
#2496=CARTESIAN_POINT ( 'NONE',  ( -17.46249999999999858, 32.54247999999999763, 0.000000000000000000 ) ) ;
#2540=CARTESIAN_POINT ( 'NONE',  ( -12.22950766483838336, -1.587500000000002132, -1.149759107507316580 ) ) ;
#2559=CIRCLE ( 'NONE', #1131, 0.3962399999999986488 ) ;
#2575=AXIS2_PLACEMENT_3D ( 'NONE', #21716, #16432, #13116 ) ;
#2651=DIRECTION ( 'NONE',  ( 0.000000000000000000, -1.000000000000000000, 0.000000000000000000 ) ) ;
#2657=ORIENTED_EDGE ( 'NONE', *, *, #3846, .T. ) ;
#2670=ADVANCED_FACE ( 'NONE', ( #5181 ), #5086, .T. ) ;
#2676=DIRECTION ( 'NONE',  ( 0.000000000000000000, 1.000000000000000000, 0.000000000000000000 ) ) ;
#2696=EDGE_CURVE ( 'NONE', #12008, #9848, #10059, .T. ) ;
#2841=ORIENTED_EDGE ( 'NONE', *, *, #11647, .T. ) ;
#2891=CARTESIAN_POINT ( 'NONE',  ( -14.35397337327049172, 34.31794000000000011, -0.6462872510839714479 ) ) ;
#2915=CIRCLE ( 'NONE', #8912, 4.961572499999999941 ) ;
#2995=EDGE_LOOP ( 'NONE', ( #11838, #1015 ) ) ;
#3007=DIRECTION ( 'NONE',  ( -0.9767031480033347979, 0.000000000000000000, 0.2145948757085687775 ) ) ;
#3035=CYLINDRICAL_SURFACE ( 'NONE', #21566, 3.175000000000001155 ) ;
#3042=CYLINDRICAL_SURFACE ( 'NONE', #2575, 3.968750000000001776 ) ;
#3053=ORIENTED_EDGE ( 'NONE', *, *, #15516, .F. ) ;
#3093=CIRCLE ( 'NONE', #15100, 5.357812499999999645 ) ;
#3140=EDGE_CURVE ( 'NONE', #5733, #17811, #3343, .T. ) ;
#3203=CIRCLE ( 'NONE', #16238, 5.357812499999999645 ) ;
#3236=EDGE_LOOP ( 'NONE', ( #18762, #4860, #20086, #3764 ) ) ;
#3337=DIRECTION ( 'NONE',  ( -0.2145948757085689163, -0.000000000000000000, -0.9767031480033347979 ) ) ;
#3343=CIRCLE ( 'NONE', #19912, 5.357812499999999645 ) ;
#3377=ORIENTED_EDGE ( 'NONE', *, *, #851, .F. ) ;
#3630=DIRECTION ( 'NONE',  ( 0.000000000000000000, 1.000000000000000000, 0.000000000000000000 ) ) ;
#3638=ORIENTED_EDGE ( 'NONE', *, *, #11278, .T. ) ;
#3677=CARTESIAN_POINT ( 'NONE',  ( -17.46249999999999858, 0.000000000000000000, 0.000000000000000000 ) ) ;
#3682=FACE_OUTER_BOUND ( 'NONE', #6468, .T. ) ;
#3744=ORIENTED_EDGE ( 'NONE', *, *, #20410, .T. ) ;
#3764=ORIENTED_EDGE ( 'NONE', *, *, #2696, .F. ) ;
#3825=DIRECTION ( 'NONE',  ( 0.000000000000000000, 1.000000000000000000, 0.000000000000000000 ) ) ;
#3846=EDGE_CURVE ( 'NONE', #17811, #1768, #21346, .T. ) ;
#3911=CIRCLE ( 'NONE', #18380, 3.175000000000001155 ) ;
#3912=DIRECTION ( 'NONE',  ( 0.000000000000000000, -1.000000000000000000, 0.000000000000000000 ) ) ;
#3934=ORIENTED_EDGE ( 'NONE', *, *, #4790, .F. ) ;
#3952=DIRECTION ( 'NONE',  ( 0.000000000000000000, 1.000000000000000000, 0.000000000000000000 ) ) ;
#4080=ORIENTED_EDGE ( 'NONE', *, *, #13166, .F. ) ;
#4155=CARTESIAN_POINT ( 'NONE',  ( -12.20004626880064080, -0.3962399999999990929, -1.006347609994785008 ) ) ;
#4157=DIRECTION ( 'NONE',  ( 0.000000000000000000, 1.000000000000000000, 0.000000000000000000 ) ) ;
#4267=( NAMED_UNIT ( * ) SI_UNIT ( $, .STERADIAN. ) SOLID_ANGLE_UNIT ( ) );
#4283=CARTESIAN_POINT ( 'NONE',  ( -17.46249999999999858, -1.983740000000001169, 0.000000000000000000 ) ) ;
#4315=VERTEX_POINT ( 'NONE', #186 ) ;
#4399=DIRECTION ( 'NONE',  ( 0.000000000000000000, -1.000000000000000000, 0.000000000000000000 ) ) ;
#4476=DIRECTION ( 'NONE',  ( 0.000000000000000000, -1.000000000000000000, 0.000000000000000000 ) ) ;
#4478=ORIENTED_EDGE ( 'NONE', *, *, #9450, .T. ) ;
#4552=ORIENTED_EDGE ( 'NONE', *, *, #18410, .F. ) ;
#4589=ORIENTED_EDGE ( 'NONE', *, *, #11647, .F. ) ;
#4658=CYLINDRICAL_SURFACE ( 'NONE', #20731, 4.365625000000000533 ) ;
#4697=CARTESIAN_POINT ( 'NONE',  ( -17.46249999999999858, 0.000000000000000000, 0.000000000000000000 ) ) ;
#4724=ORIENTED_EDGE ( 'NONE', *, *, #3140, .T. ) ;
#4790=EDGE_CURVE ( 'NONE', #4315, #12696, #16834, .T. ) ;
#4811=FACE_OUTER_BOUND ( 'NONE', #4899, .T. ) ;
#4860=ORIENTED_EDGE ( 'NONE', *, *, #851, .T. ) ;
#4899=EDGE_LOOP ( 'NONE', ( #7893, #13735, #19720, #202 ) ) ;
#4937=DIRECTION ( 'NONE',  ( -0.9790635044817342925, 0.000000000000000000, 0.2035550397114870846 ) ) ;
#4938=VERTEX_POINT ( 'NONE', #8860 ) ;
#4947=CARTESIAN_POINT ( 'NONE',  ( -22.69549233516161379, -1.587500000000002132, 1.149759107507315914 ) ) ;
#4998=DIRECTION ( 'NONE',  ( -0.9790635044817342925, 0.000000000000000000, 0.2035550397114870846 ) ) ;
#5059=FACE_BOUND ( 'NONE', #2995, .T. ) ;
#5086=PLANE ( 'NONE',  #10746 ) ;
#5103=CARTESIAN_POINT ( 'NONE',  ( -22.70813868260604096, -1.587500000000002132, 1.090609736204201763 ) ) ;
#5110=AXIS2_PLACEMENT_3D ( 'NONE', #13833, #8290, #15062 ) ;
#5181=FACE_OUTER_BOUND ( 'NONE', #13236, .T. ) ;
#5245=DIRECTION ( 'NONE',  ( 0.000000000000000000, 1.000000000000000000, 0.000000000000000000 ) ) ;
#5256=DIRECTION ( 'NONE',  ( -0.9790635044817341814, 0.000000000000000000, 0.2035550397114869736 ) ) ;
#5277=ORIENTED_EDGE ( 'NONE', *, *, #15492, .F. ) ;
#5323=AXIS2_PLACEMENT_3D ( 'NONE', #14791, #21501, #8120 ) ;
#5460=UNCERTAINTY_MEASURE_WITH_UNIT (LENGTH_MEASURE( 1.000000000000000082E-05 ), #19516, 'distance_accuracy_value', 'NONE');
#5595=CARTESIAN_POINT ( 'NONE',  ( -17.46249999999999858, -0.3962399999999990929, 0.000000000000000000 ) ) ;
#5733=VERTEX_POINT ( 'NONE', #2540 ) ;
#5770=AXIS2_PLACEMENT_3D ( 'NONE', #10913, #15801, #5828 ) ;
#5828=DIRECTION ( 'NONE',  ( -0.9790635044817342925, 0.000000000000000000, 0.2035550397114870846 ) ) ;
#5853=DIRECTION ( 'NONE',  ( 0.000000000000000000, 1.000000000000000000, 0.000000000000000000 ) ) ;
#5922=CARTESIAN_POINT ( 'NONE',  ( -17.46249999999999858, -1.587500000000002132, 0.000000000000000000 ) ) ;
#5924=PLANE ( 'NONE',  #17791 ) ;
#5950=DIRECTION ( 'NONE',  ( 0.1878280753562735217, 0.000000000000000000, 0.9822019212503905194 ) ) ;
#5967=TOROIDAL_SURFACE ( 'NONE', #19387, 4.961572499999999941, 0.3962400000000000366 ) ;
#5992=SURFACE_SIDE_STYLE ('',( #7986 ) ) ;
#6042=AXIS2_PLACEMENT_3D ( 'NONE', #17973, #1268, #1369 ) ;
#6057=DIRECTION ( 'NONE',  ( 0.9790635044817342925, 0.000000000000000000, -0.2035550397114870569 ) ) ;
#6107=SURFACE_STYLE_USAGE ( .BOTH. , #5992 ) ;
#6154=ADVANCED_FACE ( 'NONE', ( #1379 ), #10266, .T. ) ;
#6187=CARTESIAN_POINT ( 'NONE',  ( -22.72495373119935635, -0.3962399999999990929, 1.006347609994784120 ) ) ;
#6269=ORIENTED_EDGE ( 'NONE', *, *, #20987, .F. ) ;
#6279=LINE ( 'NONE', #18006, #12839 ) ;
#6303=FACE_OUTER_BOUND ( 'NONE', #21330, .T. ) ;
#6336=FACE_OUTER_BOUND ( 'NONE', #7758, .T. ) ;
#6468=EDGE_LOOP ( 'NONE', ( #3934, #4478, #7180, #1088 ) ) ;
#6512=VERTEX_POINT ( 'NONE', #9092 ) ;
#6571=CARTESIAN_POINT ( 'NONE',  ( -13.18827588824692754, 32.54247999999999763, -0.8886449702404607409 ) ) ;
#6575=MANIFOLD_SOLID_BREP ( 'Stock-MAS-676-1', #8877 ) ;
#6596=DIRECTION ( 'NONE',  ( 0.000000000000000000, 1.000000000000000000, 0.000000000000000000 ) ) ;
#6710=DIRECTION ( 'NONE',  ( -0.9790635044817341814, 0.000000000000000000, 0.2035550397114869736 ) ) ;
#6819=DIRECTION ( 'NONE',  ( 0.000000000000000000, -1.000000000000000000, 0.000000000000000000 ) ) ;
#7022=DIRECTION ( 'NONE',  ( 0.9790635044817341814, 0.000000000000000000, -0.2035550397114870014 ) ) ;
#7107=EDGE_CURVE ( 'NONE', #9848, #12344, #3911, .T. ) ;
#7118=SHAPE_DEFINITION_REPRESENTATION ( #14143, #13411 ) ;
#7141=AXIS2_PLACEMENT_3D ( 'NONE', #21645, #19647, #6057 ) ;
#7145=DIRECTION ( 'NONE',  ( 0.9790635044817341814, 0.000000000000000000, -0.2035550397114870014 ) ) ;
#7172=VERTEX_POINT ( 'NONE', #9936 ) ;
#7180=ORIENTED_EDGE ( 'NONE', *, *, #14570, .T. ) ;
#7259=CARTESIAN_POINT ( 'NONE',  ( -17.46249999999999858, -1.983740000000001169, 0.000000000000000000 ) ) ;
#7287=EDGE_LOOP ( 'NONE', ( #17893, #16910, #11273, #17341, #9871 ) ) ;
#7385=CARTESIAN_POINT ( 'NONE',  ( -17.46249999999999858, 32.54247999999999763, 0.000000000000000000 ) ) ;
#7393=AXIS2_PLACEMENT_3D ( 'NONE', #12003, #12336, #7145 ) ;
#7415=CARTESIAN_POINT ( 'NONE',  ( -17.46249999999999858, 0.000000000000000000, 0.000000000000000000 ) ) ;
#7448=( GEOMETRIC_REPRESENTATION_CONTEXT ( 3 ) GLOBAL_UNCERTAINTY_ASSIGNED_CONTEXT ( ( #8560 ) ) GLOBAL_UNIT_ASSIGNED_CONTEXT ( ( #19486, #17735, #1022 ) ) REPRESENTATION_CONTEXT ( 'NONE', 'WORKASPACE' ) );
#7457=PRODUCT_DEFINITION_CONTEXT ( 'detailed design', #13024, 'design' ) ;
#7506=EDGE_CURVE ( 'NONE', #7172, #9498, #381, .T. ) ;
#7632=ORIENTED_EDGE ( 'NONE', *, *, #20484, .T. ) ;
#7640=EDGE_CURVE ( 'NONE', #21414, #9339, #16311, .T. ) ;
#7656=ADVANCED_FACE ( 'NONE', ( #7689 ), #13234, .T. ) ;
#7689=FACE_OUTER_BOUND ( 'NONE', #16105, .T. ) ;
#7710=DIRECTION ( 'NONE',  ( 0.000000000000000000, 1.000000000000000000, 0.000000000000000000 ) ) ;
#7758=EDGE_LOOP ( 'NONE', ( #5277, #13457, #21545, #21165, #10103, #20040 ) ) ;
#7762=ORIENTED_EDGE ( 'NONE', *, *, #7506, .T. ) ;
#7790=DIRECTION ( 'NONE',  ( 0.000000000000000000, -1.000000000000000000, 0.000000000000000000 ) ) ;
#7808=FACE_OUTER_BOUND ( 'NONE', #9524, .T. ) ;
#7818=ORIENTED_EDGE ( 'NONE', *, *, #1907, .F. ) ;
#7893=ORIENTED_EDGE ( 'NONE', *, *, #18410, .T. ) ;
#7949=DIRECTION ( 'NONE',  ( 0.9822019212503901864, 0.000000000000000000, -0.1878280753562740768 ) ) ;
#7986=SURFACE_STYLE_FILL_AREA ( #14425 ) ;
#8074=FACE_OUTER_BOUND ( 'NONE', #1390, .T. ) ;
#8120=DIRECTION ( 'NONE',  ( -0.9767031480033347979, 0.000000000000000000, 0.2145948757085687775 ) ) ;
#8164=ORIENTED_EDGE ( 'NONE', *, *, #13023, .F. ) ;
#8212=AXIS2_PLACEMENT_3D ( 'NONE', #7259, #278, #13787 ) ;
#8290=DIRECTION ( 'NONE',  ( 0.000000000000000000, -1.000000000000000000, 0.000000000000000000 ) ) ;
#8317=DIRECTION ( 'NONE',  ( 0.000000000000000000, 1.000000000000000000, 0.000000000000000000 ) ) ;
#8382=CARTESIAN_POINT ( 'NONE',  ( -22.30848347979677371, -1.587500000000002132, 1.064728033956552578 ) ) ;
#8391=ORIENTED_EDGE ( 'NONE', *, *, #20331, .F. ) ;
#8453=VERTEX_POINT ( 'NONE', #6187 ) ;
#8492=DIRECTION ( 'NONE',  ( 0.2145948757085688052, 0.000000000000000000, 0.9767031480033347979 ) ) ;
#8547=VECTOR ( 'NONE', #12353, 1000.000000000000000 ) ;
#8560=UNCERTAINTY_MEASURE_WITH_UNIT (LENGTH_MEASURE( 1.000000000000000082E-05 ), #19486, 'distance_accuracy_value', 'NONE');
#8583=CIRCLE ( 'NONE', #11078, 5.357812499999999645 ) ;
#8585=DIRECTION ( 'NONE',  ( 0.000000000000000000, 1.000000000000000000, 0.000000000000000000 ) ) ;
#8607=CIRCLE ( 'NONE', #18154, 3.175000000000001155 ) ;
#8648=DIRECTION ( 'NONE',  ( -0.9790635044817341814, 0.000000000000000000, 0.2035550397114869736 ) ) ;
#8782=CARTESIAN_POINT ( 'NONE',  ( -17.46249999999999858, 33.73373999999999739, 0.000000000000000000 ) ) ;
#8793=FACE_OUTER_BOUND ( 'NONE', #14907, .T. ) ;
#8850=CIRCLE ( 'NONE', #14191, 3.175000000000001155 ) ;
#8860=CARTESIAN_POINT ( 'NONE',  ( -12.21686131739395798, -0.3962399999999990929, -1.090609736204202429 ) ) ;
#8877=CLOSED_SHELL ( 'NONE', ( #20140, #7656, #12487, #17525, #9213, #6154, #2208, #18803, #19920, #14748, #1545, #2670, #13784, #18439, #9882, #8926, #13950 ) ) ;
#8912=AXIS2_PLACEMENT_3D ( 'NONE', #14987, #9754, #21473 ) ;
#8915=AXIS2_PLACEMENT_3D ( 'NONE', #8382, #8492, #208 ) ;
#8926=ADVANCED_FACE ( 'NONE', ( #862, #21081 ), #960, .F. ) ;
#9025=CARTESIAN_POINT ( 'NONE',  ( -20.57102662672950544, 33.73373999999999739, 0.6462872510839711149 ) ) ;
#9055=ORIENTED_EDGE ( 'NONE', *, *, #16984, .T. ) ;
#9091=EDGE_CURVE ( 'NONE', #9498, #7172, #19436, .T. ) ;
#9092=CARTESIAN_POINT ( 'NONE',  ( -20.57102662672950544, 33.73373999999999739, 0.6462872510839712259 ) ) ;
#9120=EDGE_CURVE ( 'NONE', #12008, #6512, #8850, .T. ) ;
#9158=CARTESIAN_POINT ( 'NONE',  ( -22.33576604192310455, -0.3962399999999990929, 0.9319226134156143315 ) ) ;
#9198=AXIS2_PLACEMENT_3D ( 'NONE', #10563, #14020, #13680 ) ;
#9209=CARTESIAN_POINT ( 'NONE',  ( -12.58923395807689616, 5.421010862427522170E-16, -0.9319226134156151087 ) ) ;
#9213=ADVANCED_FACE ( 'NONE', ( #17309 ), #1720, .T. ) ;
#9230=DIRECTION ( 'NONE',  ( 0.9790635044817342925, 0.000000000000000000, -0.2035550397114870569 ) ) ;
#9339=VERTEX_POINT ( 'NONE', #4155 ) ;
#9342=DIRECTION ( 'NONE',  ( 0.000000000000000000, 1.000000000000000000, 0.000000000000000000 ) ) ;
#9348=EDGE_LOOP ( 'NONE', ( #1072, #15034 ) ) ;
#9389=DIRECTION ( 'NONE',  ( 0.9790635044817341814, 0.000000000000000000, -0.2035550397114870014 ) ) ;
#9424=PRESENTATION_STYLE_ASSIGNMENT (( #6107 ) ) ;
#9450=EDGE_CURVE ( 'NONE', #4315, #12574, #19803, .T. ) ;
#9498=VERTEX_POINT ( 'NONE', #6571 ) ;
#9524=EDGE_LOOP ( 'NONE', ( #3744, #1077 ) ) ;
#9641=FILL_AREA_STYLE_COLOUR ( '', #13464 ) ;
#9707=FACE_OUTER_BOUND ( 'NONE', #16370, .T. ) ;
#9736=DIRECTION ( 'NONE',  ( -0.9767031480033346869, 0.000000000000000000, 0.2145948757085690273 ) ) ;
#9754=DIRECTION ( 'NONE',  ( 0.000000000000000000, -1.000000000000000000, 0.000000000000000000 ) ) ;
#9848=VERTEX_POINT ( 'NONE', #2891 ) ;
#9862=DIRECTION ( 'NONE',  ( -0.9790635044817342925, 0.000000000000000000, 0.2035550397114870846 ) ) ;
#9871=ORIENTED_EDGE ( 'NONE', *, *, #17796, .T. ) ;
#9882=ADVANCED_FACE ( 'NONE', ( #6303 ), #4658, .T. ) ;
#9914=DIRECTION ( 'NONE',  ( -0.9790635044817342925, 0.000000000000000000, 0.2035550397114870846 ) ) ;
#9935=EDGE_LOOP ( 'NONE', ( #4552, #5 ) ) ;
#9936=CARTESIAN_POINT ( 'NONE',  ( -21.73672411175306962, 32.54247999999999763, 0.8886449702404600748 ) ) ;
#10059=LINE ( 'NONE', #18563, #13218 ) ;
#10103=ORIENTED_EDGE ( 'NONE', *, *, #16984, .F. ) ;
#10266=TOROIDAL_SURFACE ( 'NONE', #5323, 4.961572499999999941, 0.3962400000000000366 ) ;
#10337=AXIS2_PLACEMENT_3D ( 'NONE', #975, #2651, #16473 ) ;
#10344=LINE ( 'NONE', #17089, #17276 ) ;
#10437=PRODUCT_CONTEXT ( 'NONE', #10749, 'mechanical' ) ;
#10491=VERTEX_POINT ( 'NONE', #5103 ) ;
#10520=CARTESIAN_POINT ( 'NONE',  ( -12.21686131739395798, 0.000000000000000000, -1.090609736204202429 ) ) ;
#10535=CARTESIAN_POINT ( 'NONE',  ( -21.34815828341188393, 32.54247999999999763, 0.8078590638549643099 ) ) ;
#10549=DIRECTION ( 'NONE',  ( 0.000000000000000000, -1.000000000000000000, 0.000000000000000000 ) ) ;
#10563=CARTESIAN_POINT ( 'NONE',  ( -17.46249999999999858, 0.000000000000000000, 0.000000000000000000 ) ) ;
#10570=EDGE_CURVE ( 'NONE', #12696, #14357, #20385, .T. ) ;
#10673=DIRECTION ( 'NONE',  ( -0.9790635044817342925, 0.000000000000000000, 0.2035550397114870846 ) ) ;
#10685=DIRECTION ( 'NONE',  ( -0.9790635044817341814, 0.000000000000000000, 0.2035550397114869736 ) ) ;
#10746=AXIS2_PLACEMENT_3D ( 'NONE', #12047, #11834, #103 ) ;
#10749=APPLICATION_CONTEXT ( 'automotive_design' ) ;
#10769=DIRECTION ( 'NONE',  ( 0.000000000000000000, -1.000000000000000000, 0.000000000000000000 ) ) ;
#10819=ORIENTED_EDGE ( 'NONE', *, *, #20484, .F. ) ;
#10845=DIRECTION ( 'NONE',  ( -0.9790635044817341814, 0.000000000000000000, 0.2035550397114869736 ) ) ;
#10910=DIRECTION ( 'NONE',  ( 0.000000000000000000, -1.000000000000000000, 0.000000000000000000 ) ) ;
#10913=CARTESIAN_POINT ( 'NONE',  ( -17.46249999999999858, -0.3962399999999990929, 0.000000000000000000 ) ) ;
#10950=CIRCLE ( 'NONE', #1409, 5.357812499999999645 ) ;
#10955=DIRECTION ( 'NONE',  ( 0.000000000000000000, -1.000000000000000000, 0.000000000000000000 ) ) ;
#11078=AXIS2_PLACEMENT_3D ( 'NONE', #14401, #10955, #4937 ) ;
#11134=DIRECTION ( 'NONE',  ( -0.9790635044817342925, 0.000000000000000000, 0.2035550397114870846 ) ) ;
#11186=ORIENTED_EDGE ( 'NONE', *, *, #592, .T. ) ;
#11226=AXIS2_PLACEMENT_3D ( 'NONE', #7415, #17704, #10845 ) ;
#11268=CYLINDRICAL_SURFACE ( 'NONE', #11890, 3.175000000000001155 ) ;
#11273=ORIENTED_EDGE ( 'NONE', *, *, #20987, .T. ) ;
#11275=VECTOR ( 'NONE', #3630, 1000.000000000000000 ) ;
#11278=EDGE_CURVE ( 'NONE', #5733, #21341, #20059, .T. ) ;
#11319=DIRECTION ( 'NONE',  ( -0.9790635044817342925, 0.000000000000000000, 0.2035550397114870846 ) ) ;
#11469=DIRECTION ( 'NONE',  ( -0.9822019212503902974, 0.000000000000000000, 0.1878280753562734662 ) ) ;
#11534=DIRECTION ( 'NONE',  ( 0.9790635044817341814, 0.000000000000000000, -0.2035550397114870014 ) ) ;
#11637=AXIS2_PLACEMENT_3D ( 'NONE', #17209, #73, #5256 ) ;
#11643=DIRECTION ( 'NONE',  ( 0.000000000000000000, 1.000000000000000000, 0.000000000000000000 ) ) ;
#11647=EDGE_CURVE ( 'NONE', #7172, #19536, #15578, .T. ) ;
#11834=DIRECTION ( 'NONE',  ( 0.000000000000000000, 1.000000000000000000, 0.000000000000000000 ) ) ;
#11838=ORIENTED_EDGE ( 'NONE', *, *, #9120, .F. ) ;
#11857=VECTOR ( 'NONE', #20128, 1000.000000000000000 ) ;
#11890=AXIS2_PLACEMENT_3D ( 'NONE', #19444, #5853, #9389 ) ;
#11973=CARTESIAN_POINT ( 'NONE',  ( -17.46249999999999858, 32.54247999999999763, 0.000000000000000000 ) ) ;
#12003=CARTESIAN_POINT ( 'NONE',  ( -17.46249999999999858, 33.73373999999999739, 0.000000000000000000 ) ) ;
#12004=DIRECTION ( 'NONE',  ( 0.9790635044817342925, 0.000000000000000000, -0.2035550397114870569 ) ) ;
#12008=VERTEX_POINT ( 'NONE', #20952 ) ;
#12045=AXIS2_PLACEMENT_3D ( 'NONE', #2496, #4157, #9230 ) ;
#12047=CARTESIAN_POINT ( 'NONE',  ( -17.46249999999999858, 34.31794000000000011, 0.000000000000000000 ) ) ;
#12121=ORIENTED_EDGE ( 'NONE', *, *, #11278, .F. ) ;
#12229=DIRECTION ( 'NONE',  ( -0.9790635044817342925, 0.000000000000000000, 0.2035550397114870846 ) ) ;
#12316=AXIS2_PLACEMENT_3D ( 'NONE', #15070, #3337, #9736 ) ;
#12336=DIRECTION ( 'NONE',  ( 0.000000000000000000, 1.000000000000000000, 0.000000000000000000 ) ) ;
#12344=VERTEX_POINT ( 'NONE', #20134 ) ;
#12353=DIRECTION ( 'NONE',  ( 0.000000000000000000, 1.000000000000000000, 0.000000000000000000 ) ) ;
#12397=TOROIDAL_SURFACE ( 'NONE', #13451, 4.961572499999999941, 0.3962400000000000366 ) ;
#12487=ADVANCED_FACE ( 'NONE', ( #984 ), #11268, .T. ) ;
#12574=VERTEX_POINT ( 'NONE', #16373 ) ;
#12658=CARTESIAN_POINT ( 'NONE',  ( -12.61651652020322523, -1.983740000000001613, -1.064728033956553244 ) ) ;
#12683=VECTOR ( 'NONE', #3912, 1000.000000000000000 ) ;
#12696=VERTEX_POINT ( 'NONE', #15150 ) ;
#12775=AXIS2_PLACEMENT_3D ( 'NONE', #21059, #7790, #10685 ) ;
#12835=DIRECTION ( 'NONE',  ( 0.000000000000000000, -1.000000000000000000, 0.000000000000000000 ) ) ;
#12839=VECTOR ( 'NONE', #12835, 1000.000000000000000 ) ;
#12862=AXIS2_PLACEMENT_3D ( 'NONE', #15461, #6819, #6710 ) ;
#12906=( NAMED_UNIT ( * ) PLANE_ANGLE_UNIT ( ) SI_UNIT ( $, .RADIAN. ) );
#12911=CARTESIAN_POINT ( 'NONE',  ( -22.30848347979677371, -1.983740000000001613, 1.064728033956552800 ) ) ;
#12959=DIRECTION ( 'NONE',  ( 0.9790635044817341814, 0.000000000000000000, -0.2035550397114870014 ) ) ;
#12968=CARTESIAN_POINT ( 'NONE',  ( -17.46249999999999858, 32.54247999999999763, 0.000000000000000000 ) ) ;
#13023=EDGE_CURVE ( 'NONE', #8453, #20325, #21085, .T. ) ;
#13024=APPLICATION_CONTEXT ( 'automotive_design' ) ;
#13116=DIRECTION ( 'NONE',  ( -0.9790635044817341814, 0.000000000000000000, 0.2035550397114869736 ) ) ;
#13166=EDGE_CURVE ( 'NONE', #10491, #5733, #3093, .T. ) ;
#13218=VECTOR ( 'NONE', #16903, 1000.000000000000000 ) ;
#13234=CYLINDRICAL_SURFACE ( 'NONE', #16981, 4.365625000000000533 ) ;
#13236=EDGE_LOOP ( 'NONE', ( #636, #17368 ) ) ;
#13357=DIRECTION ( 'NONE',  ( 0.9790635044817342925, 0.000000000000000000, -0.2035550397114870569 ) ) ;
#13393=DIRECTION ( 'NONE',  ( 0.9790635044817342925, 0.000000000000000000, -0.2035550397114870569 ) ) ;
#13411=SHAPE_REPRESENTATION ( 'Pivot Pin', ( #2234 ), #15867 ) ;
#13451=AXIS2_PLACEMENT_3D ( 'NONE', #16559, #1827, #11469 ) ;
#13457=ORIENTED_EDGE ( 'NONE', *, *, #13636, .F. ) ;
#13464=COLOUR_RGB ( '', 0.40784314, 0.44705882, 0.49803922) ;
#13636=EDGE_CURVE ( 'NONE', #9339, #4938, #10950, .T. ) ;
#13680=DIRECTION ( 'NONE',  ( -0.9790635044817342925, 0.000000000000000000, 0.2035550397114870846 ) ) ;
#13717=EDGE_CURVE ( 'NONE', #21414, #17151, #21196, .T. ) ;
#13735=ORIENTED_EDGE ( 'NONE', *, *, #4790, .T. ) ;
#13784=ADVANCED_FACE ( 'NONE', ( #1152 ), #3035, .T. ) ;
#13787=DIRECTION ( 'NONE',  ( -0.9790635044817342925, 0.000000000000000000, 0.2035550397114870846 ) ) ;
#13824=ORIENTED_EDGE ( 'NONE', *, *, #17671, .T. ) ;
#13827=ORIENTED_EDGE ( 'NONE', *, *, #13166, .T. ) ;
#13833=CARTESIAN_POINT ( 'NONE',  ( -17.46249999999999858, -1.587500000000002132, 0.000000000000000000 ) ) ;
#13950=ADVANCED_FACE ( 'NONE', ( #3682 ), #17275, .T. ) ;
#14020=DIRECTION ( 'NONE',  ( 0.000000000000000000, -1.000000000000000000, 0.000000000000000000 ) ) ;
#14022=CARTESIAN_POINT ( 'NONE',  ( 0.000000000000000000, 0.000000000000000000, 0.000000000000000000 ) ) ;
#14062=CARTESIAN_POINT ( 'NONE',  ( -13.18827588824692754, 33.73373999999999739, -0.8886449702404607409 ) ) ;
#14143=PRODUCT_DEFINITION_SHAPE ( 'NONE', 'NONE',  #19378 ) ;
#14146=CIRCLE ( 'NONE', #11637, 3.968750000000001776 ) ;
#14163=TOROIDAL_SURFACE ( 'NONE', #19772, 4.961572499999999941, 0.3962400000000000366 ) ;
#14191=AXIS2_PLACEMENT_3D ( 'NONE', #8782, #20724, #7022 ) ;
#14214=CARTESIAN_POINT ( 'NONE',  ( -17.46249999999999858, -0.3962399999999990929, 0.000000000000000000 ) ) ;
#14278=PRODUCT ( 'Pivot Pin', 'Pivot Pin', '', ( #10437 ) ) ;
#14333=CARTESIAN_POINT ( 'NONE',  ( -17.46249999999999858, -0.3962399999999990929, 0.000000000000000000 ) ) ;
#14356=DIRECTION ( 'NONE',  ( -0.9790635044817342925, 0.000000000000000000, 0.2035550397114870846 ) ) ;
#14357=VERTEX_POINT ( 'NONE', #18043 ) ;
#14401=CARTESIAN_POINT ( 'NONE',  ( -17.46249999999999858, -1.587500000000002132, 0.000000000000000000 ) ) ;
#14425=FILL_AREA_STYLE ('',( #9641 ) ) ;
#14470=DIRECTION ( 'NONE',  ( -0.2035550397114870846, 0.000000000000000000, -0.9790635044817342925 ) ) ;
#14488=FACE_BOUND ( 'NONE', #20647, .T. ) ;
#14570=EDGE_CURVE ( 'NONE', #12574, #14357, #15655, .T. ) ;
#14623=CARTESIAN_POINT ( 'NONE',  ( -17.46249999999999858, 34.31794000000000011, 0.000000000000000000 ) ) ;
#14678=ORIENTED_EDGE ( 'NONE', *, *, #10570, .T. ) ;
#14679=SHAPE_REPRESENTATION_RELATIONSHIP ( 'NONE' , 'NONE' ,  #13411, #15909 ) ;
#14748=ADVANCED_FACE ( 'NONE', ( #16297 ), #5967, .T. ) ;
#14791=CARTESIAN_POINT ( 'NONE',  ( -17.46249999999999858, -1.587500000000002132, 0.000000000000000000 ) ) ;
#14797=ORIENTED_EDGE ( 'NONE', *, *, #17784, .T. ) ;
#14907=EDGE_LOOP ( 'NONE', ( #11186, #18774 ) ) ;
#14987=CARTESIAN_POINT ( 'NONE',  ( -17.46249999999999858, -1.983740000000001169, 0.000000000000000000 ) ) ;
#15034=ORIENTED_EDGE ( 'NONE', *, *, #7506, .F. ) ;
#15062=DIRECTION ( 'NONE',  ( -0.9790635044817342925, 0.000000000000000000, 0.2035550397114870846 ) ) ;
#15070=CARTESIAN_POINT ( 'NONE',  ( -12.61651652020322523, -1.587500000000002132, -1.064728033956553244 ) ) ;
#15076=ORIENTED_EDGE ( 'NONE', *, *, #13717, .T. ) ;
#15093=DIRECTION ( 'NONE',  ( 0.000000000000000000, 1.000000000000000000, 0.000000000000000000 ) ) ;
#15100=AXIS2_PLACEMENT_3D ( 'NONE', #5922, #10910, #14356 ) ;
#15150=CARTESIAN_POINT ( 'NONE',  ( -13.57684171658811678, 0.000000000000000000, -0.8078590638549644209 ) ) ;
#15234=MECHANICAL_DESIGN_GEOMETRIC_PRESENTATION_REPRESENTATION('',(#20),#7448);
#15255=CARTESIAN_POINT ( 'NONE',  ( -21.73672411175306962, 33.73373999999999739, 0.8886449702404600748 ) ) ;
#15295=CIRCLE ( 'NONE', #8212, 4.961572499999999941 ) ;
#15343=FACE_OUTER_BOUND ( 'NONE', #18073, .T. ) ;
#15359=DIRECTION ( 'NONE',  ( -0.2035550397114870846, 0.000000000000000000, -0.9790635044817342925 ) ) ;
#15461=CARTESIAN_POINT ( 'NONE',  ( -17.46249999999999858, 0.000000000000000000, 0.000000000000000000 ) ) ;
#15471=DIRECTION ( 'NONE',  ( -0.9790635044817342925, 0.000000000000000000, 0.2035550397114870846 ) ) ;
#15492=EDGE_CURVE ( 'NONE', #4938, #17811, #19463, .T. ) ;
#15516=EDGE_CURVE ( 'NONE', #12344, #9848, #8607, .T. ) ;
#15578=LINE ( 'NONE', #17117, #11275 ) ;
#15655=LINE ( 'NONE', #10535, #12683 ) ;
#15660=CIRCLE ( 'NONE', #8915, 0.3962400000000012579 ) ;
#15663=CIRCLE ( 'NONE', #1520, 4.961572499999999941 ) ;
#15801=DIRECTION ( 'NONE',  ( 0.000000000000000000, 1.000000000000000000, 0.000000000000000000 ) ) ;
#15825=ORIENTED_EDGE ( 'NONE', *, *, #1487, .F. ) ;
#15867=( GEOMETRIC_REPRESENTATION_CONTEXT ( 3 ) GLOBAL_UNCERTAINTY_ASSIGNED_CONTEXT ( ( #5460 ) ) GLOBAL_UNIT_ASSIGNED_CONTEXT ( ( #19516, #12906, #4267 ) ) REPRESENTATION_CONTEXT ( 'NONE', 'WORKASPACE' ) );
#15909=ADVANCED_BREP_SHAPE_REPRESENTATION ( '', ( #6575, #2234 ), #15867 ) ;
#15913=AXIS2_PLACEMENT_3D ( 'NONE', #1844, #8585, #15359 ) ;
#15976=ORIENTED_EDGE ( 'NONE', *, *, #2696, .T. ) ;
#16011=CIRCLE ( 'NONE', #76, 4.365625000000000533 ) ;
#16105=EDGE_LOOP ( 'NONE', ( #18233, #2841, #309, #19949 ) ) ;
#16128=VERTEX_POINT ( 'NONE', #12911 ) ;
#16238=AXIS2_PLACEMENT_3D ( 'NONE', #17194, #17305, #12229 ) ;
#16297=FACE_OUTER_BOUND ( 'NONE', #7287, .T. ) ;
#16311=CIRCLE ( 'NONE', #6042, 0.3962400000000003142 ) ;
#16370=EDGE_LOOP ( 'NONE', ( #21623, #15076 ) ) ;
#16373=CARTESIAN_POINT ( 'NONE',  ( -21.34815828341188393, 32.54247999999999763, 0.8078590638549643099 ) ) ;
#16392=VECTOR ( 'NONE', #17266, 1000.000000000000000 ) ;
#16432=DIRECTION ( 'NONE',  ( 0.000000000000000000, -1.000000000000000000, 0.000000000000000000 ) ) ;
#16473=DIRECTION ( 'NONE',  ( -0.9790635044817342925, 0.000000000000000000, 0.2035550397114870846 ) ) ;
#16496=CARTESIAN_POINT ( 'NONE',  ( -17.46249999999999858, -1.587500000000002132, 0.000000000000000000 ) ) ;
#16559=CARTESIAN_POINT ( 'NONE',  ( -17.46249999999999858, -0.3962399999999990929, 0.000000000000000000 ) ) ;
#16617=EDGE_LOOP ( 'NONE', ( #3377, #13824, #15976, #3053 ) ) ;
#16834=LINE ( 'NONE', #18375, #11857 ) ;
#16903=DIRECTION ( 'NONE',  ( 0.000000000000000000, 1.000000000000000000, 0.000000000000000000 ) ) ;
#16910=ORIENTED_EDGE ( 'NONE', *, *, #21709, .F. ) ;
#16960=ORIENTED_EDGE ( 'NONE', *, *, #20410, .F. ) ;
#16973=ORIENTED_EDGE ( 'NONE', *, *, #15492, .T. ) ;
#16981=AXIS2_PLACEMENT_3D ( 'NONE', #17764, #9342, #18195 ) ;
#16984=EDGE_CURVE ( 'NONE', #1768, #10491, #8583, .T. ) ;
#16989=PLANE ( 'NONE',  #15913 ) ;
#17059=CIRCLE ( 'NONE', #5770, 5.357812499999999645 ) ;
#17089=CARTESIAN_POINT ( 'NONE',  ( -13.18827588824692754, 32.54247999999999763, -0.8886449702404607409 ) ) ;
#17117=CARTESIAN_POINT ( 'NONE',  ( -21.73672411175306962, 32.54247999999999763, 0.8886449702404602968 ) ) ;
#17151=VERTEX_POINT ( 'NONE', #2045 ) ;
#17194=CARTESIAN_POINT ( 'NONE',  ( -17.46249999999999858, -0.3962399999999990929, 0.000000000000000000 ) ) ;
#17209=CARTESIAN_POINT ( 'NONE',  ( -17.46249999999999858, 32.54247999999999763, 0.000000000000000000 ) ) ;
#17237=EDGE_CURVE ( 'NONE', #14357, #12696, #21308, .T. ) ;
#17266=DIRECTION ( 'NONE',  ( 0.000000000000000000, -1.000000000000000000, 0.000000000000000000 ) ) ;
#17275=CYLINDRICAL_SURFACE ( 'NONE', #17347, 3.968750000000001776 ) ;
#17276=VECTOR ( 'NONE', #3825, 1000.000000000000000 ) ;
#17305=DIRECTION ( 'NONE',  ( 0.000000000000000000, 1.000000000000000000, 0.000000000000000000 ) ) ;
#17309=FACE_OUTER_BOUND ( 'NONE', #20662, .T. ) ;
#17341=ORIENTED_EDGE ( 'NONE', *, *, #13023, .T. ) ;
#17347=AXIS2_PLACEMENT_3D ( 'NONE', #11973, #1789, #8648 ) ;
#17368=ORIENTED_EDGE ( 'NONE', *, *, #15516, .T. ) ;
#17443=LINE ( 'NONE', #9025, #8547 ) ;
#17525=ADVANCED_FACE ( 'NONE', ( #15343 ), #12397, .T. ) ;
#17644=DIRECTION ( 'NONE',  ( 1.000000000000000000, 0.000000000000000000, 0.000000000000000000 ) ) ;
#17671=EDGE_CURVE ( 'NONE', #6512, #12008, #2134, .T. ) ;
#17686=AXIS2_PLACEMENT_3D ( 'NONE', #19858, #6596, #13357 ) ;
#17704=DIRECTION ( 'NONE',  ( 0.000000000000000000, -1.000000000000000000, 0.000000000000000000 ) ) ;
#17735=( NAMED_UNIT ( * ) PLANE_ANGLE_UNIT ( ) SI_UNIT ( $, .RADIAN. ) );
#17764=CARTESIAN_POINT ( 'NONE',  ( -17.46249999999999858, 32.54247999999999763, 0.000000000000000000 ) ) ;
#17784=EDGE_CURVE ( 'NONE', #9498, #19225, #10344, .T. ) ;
#17791=AXIS2_PLACEMENT_3D ( 'NONE', #4283, #4399, #11134 ) ;
#17796=EDGE_CURVE ( 'NONE', #20325, #9339, #3203, .T. ) ;
#17811=VERTEX_POINT ( 'NONE', #21274 ) ;
#17893=ORIENTED_EDGE ( 'NONE', *, *, #7640, .F. ) ;
#17973=CARTESIAN_POINT ( 'NONE',  ( -12.58923395807689616, -0.3962399999999990929, -0.9319226134156148866 ) ) ;
#18006=CARTESIAN_POINT ( 'NONE',  ( -22.70813868260604096, 0.000000000000000000, 1.090609736204201763 ) ) ;
#18030=CARTESIAN_POINT ( 'NONE',  ( -17.46249999999999858, 34.31794000000000011, 0.000000000000000000 ) ) ;
#18043=CARTESIAN_POINT ( 'NONE',  ( -21.34815828341188393, 0.000000000000000000, 0.8078590638549643099 ) ) ;
#18073=EDGE_LOOP ( 'NONE', ( #21735, #803, #19989, #18718, #6269 ) ) ;
#18154=AXIS2_PLACEMENT_3D ( 'NONE', #18030, #2676, #21670 ) ;
#18195=DIRECTION ( 'NONE',  ( 0.9790635044817342925, 0.000000000000000000, -0.2035550397114870569 ) ) ;
#18233=ORIENTED_EDGE ( 'NONE', *, *, #9091, .T. ) ;
#18375=CARTESIAN_POINT ( 'NONE',  ( -13.57684171658811501, 32.54247999999999763, -0.8078590638549647540 ) ) ;
#18380=AXIS2_PLACEMENT_3D ( 'NONE', #14623, #21332, #12959 ) ;
#18410=EDGE_CURVE ( 'NONE', #12574, #4315, #14146, .T. ) ;
#18439=ADVANCED_FACE ( 'NONE', ( #5059, #8793 ), #16989, .T. ) ;
#18563=CARTESIAN_POINT ( 'NONE',  ( -14.35397337327049172, 33.73373999999999739, -0.6462872510839714479 ) ) ;
#18718=ORIENTED_EDGE ( 'NONE', *, *, #1907, .T. ) ;
#18762=ORIENTED_EDGE ( 'NONE', *, *, #9120, .T. ) ;
#18774=ORIENTED_EDGE ( 'NONE', *, *, #20331, .T. ) ;
#18803=ADVANCED_FACE ( 'NONE', ( #8074 ), #14163, .T. ) ;
#18849=CARTESIAN_POINT ( 'NONE',  ( -22.70813868260604096, -0.3962399999999990929, 1.090609736204201763 ) ) ;
#19225=VERTEX_POINT ( 'NONE', #14062 ) ;
#19307=ORIENTED_EDGE ( 'NONE', *, *, #17237, .T. ) ;
#19378=PRODUCT_DEFINITION ( 'UNKNOWN', '', #1706, #7457 ) ;
#19387=AXIS2_PLACEMENT_3D ( 'NONE', #14214, #10769, #19483 ) ;
#19436=CIRCLE ( 'NONE', #17686, 4.365625000000000533 ) ;
#19444=CARTESIAN_POINT ( 'NONE',  ( -17.46249999999999858, 33.73373999999999739, 0.000000000000000000 ) ) ;
#19463=LINE ( 'NONE', #10520, #16392 ) ;
#19483=DIRECTION ( 'NONE',  ( -0.9822019212503902974, 0.000000000000000000, 0.1878280753562734662 ) ) ;
#19486=( LENGTH_UNIT ( ) NAMED_UNIT ( * ) SI_UNIT ( .MILLI., .METRE. ) );
#19516=( LENGTH_UNIT ( ) NAMED_UNIT ( * ) SI_UNIT ( .MILLI., .METRE. ) );
#19536=VERTEX_POINT ( 'NONE', #15255 ) ;
#19647=DIRECTION ( 'NONE',  ( 0.000000000000000000, 1.000000000000000000, 0.000000000000000000 ) ) ;
#19720=ORIENTED_EDGE ( 'NONE', *, *, #17237, .F. ) ;
#19772=AXIS2_PLACEMENT_3D ( 'NONE', #16496, #1119, #3007 ) ;
#19803=CIRCLE ( 'NONE', #12775, 3.968750000000001776 ) ;
#19858=CARTESIAN_POINT ( 'NONE',  ( -17.46249999999999858, 32.54247999999999763, 0.000000000000000000 ) ) ;
#19912=AXIS2_PLACEMENT_3D ( 'NONE', #2144, #10549, #9914 ) ;
#19920=ADVANCED_FACE ( 'NONE', ( #6336 ), #1257, .T. ) ;
#19949=ORIENTED_EDGE ( 'NONE', *, *, #17784, .F. ) ;
#19989=ORIENTED_EDGE ( 'NONE', *, *, #13636, .T. ) ;
#20027=CARTESIAN_POINT ( 'NONE',  ( -17.46249999999999858, 0.000000000000000000, 0.000000000000000000 ) ) ;
#20040=ORIENTED_EDGE ( 'NONE', *, *, #3846, .F. ) ;
#20059=CIRCLE ( 'NONE', #12316, 0.3962399999999995925 ) ;
#20086=ORIENTED_EDGE ( 'NONE', *, *, #7107, .F. ) ;
#20128=DIRECTION ( 'NONE',  ( 0.000000000000000000, -1.000000000000000000, 0.000000000000000000 ) ) ;
#20134=CARTESIAN_POINT ( 'NONE',  ( -20.57102662672950544, 34.31794000000000011, 0.6462872510839712259 ) ) ;
#20140=ADVANCED_FACE ( 'NONE', ( #4811 ), #3042, .T. ) ;
#20191=AXIS2_PLACEMENT_3D ( 'NONE', #4697, #4476, #9862 ) ;
#20204=EDGE_LOOP ( 'NONE', ( #9055, #13827, #3638, #16960, #10819 ) ) ;
#20272=ORIENTED_EDGE ( 'NONE', *, *, #3140, .F. ) ;
#20325=VERTEX_POINT ( 'NONE', #18849 ) ;
#20331=EDGE_CURVE ( 'NONE', #19536, #19225, #16011, .T. ) ;
#20352=AXIS2_PLACEMENT_3D ( 'NONE', #5595, #3952, #15471 ) ;
#20385=CIRCLE ( 'NONE', #11226, 3.968750000000001776 ) ;
#20410=EDGE_CURVE ( 'NONE', #16128, #21341, #15295, .T. ) ;
#20473=AXIS2_PLACEMENT_3D ( 'NONE', #20027, #11643, #11319 ) ;
#20484=EDGE_CURVE ( 'NONE', #1768, #16128, #15660, .T. ) ;
#20647=EDGE_LOOP ( 'NONE', ( #19307, #14678 ) ) ;
#20662=EDGE_LOOP ( 'NONE', ( #7818, #16973, #20272, #4080, #15825, #8164 ) ) ;
#20724=DIRECTION ( 'NONE',  ( 0.000000000000000000, 1.000000000000000000, 0.000000000000000000 ) ) ;
#20731=AXIS2_PLACEMENT_3D ( 'NONE', #12968, #21446, #13393 ) ;
#20952=CARTESIAN_POINT ( 'NONE',  ( -14.35397337327049172, 33.73373999999999739, -0.6462872510839714479 ) ) ;
#20987=EDGE_CURVE ( 'NONE', #17151, #8453, #2559, .T. ) ;
#21049=DIRECTION ( 'NONE',  ( 0.000000000000000000, 1.000000000000000000, 0.000000000000000000 ) ) ;
#21059=CARTESIAN_POINT ( 'NONE',  ( -17.46249999999999858, 32.54247999999999763, 0.000000000000000000 ) ) ;
#21081=FACE_OUTER_BOUND ( 'NONE', #9348, .T. ) ;
#21085=CIRCLE ( 'NONE', #20352, 5.357812499999999645 ) ;
#21165=ORIENTED_EDGE ( 'NONE', *, *, #1487, .T. ) ;
#21196=CIRCLE ( 'NONE', #20473, 4.961572499999999941 ) ;
#21274=CARTESIAN_POINT ( 'NONE',  ( -12.21686131739395798, -1.587500000000002132, -1.090609736204202429 ) ) ;
#21308=CIRCLE ( 'NONE', #12862, 3.968750000000001776 ) ;
#21330=EDGE_LOOP ( 'NONE', ( #4589, #7762, #14797, #8391 ) ) ;
#21332=DIRECTION ( 'NONE',  ( 0.000000000000000000, 1.000000000000000000, 0.000000000000000000 ) ) ;
#21341=VERTEX_POINT ( 'NONE', #12658 ) ;
#21346=CIRCLE ( 'NONE', #5110, 5.357812499999999645 ) ;
#21373=CARTESIAN_POINT ( 'NONE',  ( -17.46249999999999858, 33.73373999999999739, 0.000000000000000000 ) ) ;
#21414=VERTEX_POINT ( 'NONE', #9209 ) ;
#21446=DIRECTION ( 'NONE',  ( 0.000000000000000000, 1.000000000000000000, 0.000000000000000000 ) ) ;
#21473=DIRECTION ( 'NONE',  ( -0.9790635044817342925, 0.000000000000000000, 0.2035550397114870846 ) ) ;
#21501=DIRECTION ( 'NONE',  ( 0.000000000000000000, -1.000000000000000000, 0.000000000000000000 ) ) ;
#21545=ORIENTED_EDGE ( 'NONE', *, *, #17796, .F. ) ;
#21566=AXIS2_PLACEMENT_3D ( 'NONE', #21373, #15093, #11534 ) ;
#21623=ORIENTED_EDGE ( 'NONE', *, *, #21709, .T. ) ;
#21645=CARTESIAN_POINT ( 'NONE',  ( -17.46249999999999858, 33.73373999999999739, 0.000000000000000000 ) ) ;
#21670=DIRECTION ( 'NONE',  ( 0.9790635044817341814, 0.000000000000000000, -0.2035550397114870014 ) ) ;
#21709=EDGE_CURVE ( 'NONE', #17151, #21414, #15663, .T. ) ;
#21716=CARTESIAN_POINT ( 'NONE',  ( -17.46249999999999858, 32.54247999999999763, 0.000000000000000000 ) ) ;
#21735=ORIENTED_EDGE ( 'NONE', *, *, #13717, .F. ) ;
ENDSEC;
END-ISO-10303-21;
